ISO-10303-21;
HEADER;
/* Generated by software containing ST-Developer
 * from STEP Tools, Inc. (www.steptools.com) 
 */

FILE_DESCRIPTION(
/* description */ ('Round-Shaft Linear Stage with Ball Bushings'),
/* implementation_level */ '2;1');

FILE_NAME(
/* name */ 'Cap Screw - M5x20.step',
/* time_stamp */ '2026-10-27T10:47:55-07:00',
/* author */ (''),
/* organization */ (''),
/* preprocessor_version */ 'ST-DEVELOPER v20.2',
/* originating_system */ 'Autodesk Translation Framework v15.17.0.0',
/* authorisation */ '');

FILE_SCHEMA (('AUTOMOTIVE_DESIGN { 1 0 10303 214 3 1 1 }'));
ENDSEC;

DATA;
#10=MECHANICAL_DESIGN_GEOMETRIC_PRESENTATION_REPRESENTATION('',(#320),#7835);
#237=ORIENTED_CLOSED_SHELL('',*,#4413,.F.);
#241=BREP_WITH_VOIDS('Body1',#4412,(#237));
#252=CONICAL_SURFACE('',#5064,0.4,0.785398163397448);
#253=CONICAL_SURFACE('',#5068,0.41,0.785398163397448);
#254=CONICAL_SURFACE('',#5072,0.26,0.463647609000806);
#255=CONICAL_SURFACE('',#5076,0.225,0.785398163397448);
#278=SHAPE_REPRESENTATION_RELATIONSHIP('SRR','None',#7968,#299);
#299=ADVANCED_BREP_SHAPE_REPRESENTATION('',(#241),#7832);
#320=STYLED_ITEM('',(#8151),#241);
#455=FACE_BOUND('',#1212,.T.);
#592=PLANE('',#5062);
#593=PLANE('',#5070);
#594=PLANE('',#5078);
#595=PLANE('',#5079);
#596=PLANE('',#5080);
#597=PLANE('',#5081);
#598=PLANE('',#5082);
#599=PLANE('',#5083);
#600=PLANE('',#5084);
#601=PLANE('',#5085);
#602=PLANE('',#5086);
#835=FACE_OUTER_BOUND('',#1207,.T.);
#836=FACE_OUTER_BOUND('',#1208,.T.);
#837=FACE_OUTER_BOUND('',#1209,.T.);
#838=FACE_OUTER_BOUND('',#1210,.T.);
#839=FACE_OUTER_BOUND('',#1211,.T.);
#840=FACE_OUTER_BOUND('',#1213,.T.);
#841=FACE_OUTER_BOUND('',#1214,.T.);
#842=FACE_OUTER_BOUND('',#1215,.T.);
#843=FACE_OUTER_BOUND('',#1216,.T.);
#844=FACE_OUTER_BOUND('',#1217,.T.);
#845=FACE_OUTER_BOUND('',#1218,.T.);
#846=FACE_OUTER_BOUND('',#1219,.T.);
#847=FACE_OUTER_BOUND('',#1220,.T.);
#848=FACE_OUTER_BOUND('',#1221,.T.);
#849=FACE_OUTER_BOUND('',#1222,.T.);
#850=FACE_OUTER_BOUND('',#1223,.T.);
#851=FACE_OUTER_BOUND('',#1224,.T.);
#1207=EDGE_LOOP('',(#3912));
#1208=EDGE_LOOP('',(#3913,#3914,#3915,#3916));
#1209=EDGE_LOOP('',(#3917,#3918,#3919,#3920));
#1210=EDGE_LOOP('',(#3921,#3922,#3923,#3924));
#1211=EDGE_LOOP('',(#3925));
#1212=EDGE_LOOP('',(#3926));
#1213=EDGE_LOOP('',(#3927,#3928,#3929,#3930));
#1214=EDGE_LOOP('',(#3931,#3932,#3933,#3934));
#1215=EDGE_LOOP('',(#3935,#3936,#3937,#3938));
#1216=EDGE_LOOP('',(#3939));
#1217=EDGE_LOOP('',(#3940,#3941,#3942,#3943));
#1218=EDGE_LOOP('',(#3944,#3945,#3946,#3947));
#1219=EDGE_LOOP('',(#3948,#3949,#3950,#3951));
#1220=EDGE_LOOP('',(#3952,#3953,#3954,#3955));
#1221=EDGE_LOOP('',(#3956,#3957,#3958,#3959));
#1222=EDGE_LOOP('',(#3960,#3961,#3962,#3963));
#1223=EDGE_LOOP('',(#3964,#3965,#3966,#3967,#3968,#3969));
#1224=EDGE_LOOP('',(#3970,#3971,#3972,#3973,#3974,#3975));
#1539=LINE('',#7582,#1879);
#1540=LINE('',#7586,#1880);
#1541=LINE('',#7590,#1881);
#1542=LINE('',#7597,#1882);
#1543=LINE('',#7601,#1883);
#1544=LINE('',#7605,#1884);
#1545=LINE('',#7610,#1885);
#1546=LINE('',#7612,#1886);
#1547=LINE('',#7614,#1887);
#1548=LINE('',#7615,#1888);
#1549=LINE('',#7618,#1889);
#1550=LINE('',#7620,#1890);
#1551=LINE('',#7621,#1891);
#1552=LINE('',#7624,#1892);
#1553=LINE('',#7626,#1893);
#1554=LINE('',#7627,#1894);
#1555=LINE('',#7630,#1895);
#1556=LINE('',#7632,#1896);
#1557=LINE('',#7633,#1897);
#1558=LINE('',#7636,#1898);
#1559=LINE('',#7638,#1899);
#1560=LINE('',#7639,#1900);
#1561=LINE('',#7641,#1901);
#1562=LINE('',#7642,#1902);
#1879=VECTOR('',#6300,0.4);
#1880=VECTOR('',#6305,0.425);
#1881=VECTOR('',#6310,0.41);
#1882=VECTOR('',#6319,0.26);
#1883=VECTOR('',#6324,0.25);
#1884=VECTOR('',#6329,0.225);
#1885=VECTOR('',#6334,1.);
#1886=VECTOR('',#6335,1.);
#1887=VECTOR('',#6336,1.);
#1888=VECTOR('',#6337,1.);
#1889=VECTOR('',#6340,1.);
#1890=VECTOR('',#6341,1.);
#1891=VECTOR('',#6342,1.);
#1892=VECTOR('',#6345,1.);
#1893=VECTOR('',#6346,1.);
#1894=VECTOR('',#6347,1.);
#1895=VECTOR('',#6350,1.);
#1896=VECTOR('',#6351,1.);
#1897=VECTOR('',#6352,1.);
#1898=VECTOR('',#6355,1.);
#1899=VECTOR('',#6356,1.);
#1900=VECTOR('',#6357,1.);
#1901=VECTOR('',#6360,1.);
#1902=VECTOR('',#6361,1.);
#2098=CIRCLE('',#5063,0.375);
#2099=CIRCLE('',#5065,0.425);
#2100=CIRCLE('',#5067,0.425);
#2101=CIRCLE('',#5069,0.395);
#2102=CIRCLE('',#5071,0.27);
#2103=CIRCLE('',#5073,0.24505);
#2104=CIRCLE('',#5075,0.24505);
#2105=CIRCLE('',#5077,0.2);
#2421=VERTEX_POINT('',#7577);
#2422=VERTEX_POINT('',#7580);
#2423=VERTEX_POINT('',#7584);
#2424=VERTEX_POINT('',#7588);
#2425=VERTEX_POINT('',#7592);
#2426=VERTEX_POINT('',#7595);
#2427=VERTEX_POINT('',#7599);
#2428=VERTEX_POINT('',#7603);
#2429=VERTEX_POINT('',#7608);
#2430=VERTEX_POINT('',#7609);
#2431=VERTEX_POINT('',#7611);
#2432=VERTEX_POINT('',#7613);
#2433=VERTEX_POINT('',#7617);
#2434=VERTEX_POINT('',#7619);
#2435=VERTEX_POINT('',#7623);
#2436=VERTEX_POINT('',#7625);
#2437=VERTEX_POINT('',#7629);
#2438=VERTEX_POINT('',#7631);
#2439=VERTEX_POINT('',#7635);
#2440=VERTEX_POINT('',#7637);
#2924=EDGE_CURVE('',#2421,#2421,#2098,.T.);
#2925=EDGE_CURVE('',#2422,#2422,#2099,.T.);
#2926=EDGE_CURVE('',#2422,#2421,#1539,.T.);
#2927=EDGE_CURVE('',#2423,#2423,#2100,.T.);
#2928=EDGE_CURVE('',#2423,#2422,#1540,.T.);
#2929=EDGE_CURVE('',#2424,#2424,#2101,.T.);
#2930=EDGE_CURVE('',#2424,#2423,#1541,.T.);
#2931=EDGE_CURVE('',#2425,#2425,#2102,.T.);
#2932=EDGE_CURVE('',#2426,#2426,#2103,.F.);
#2933=EDGE_CURVE('',#2426,#2425,#1542,.T.);
#2934=EDGE_CURVE('',#2427,#2427,#2104,.F.);
#2935=EDGE_CURVE('',#2427,#2426,#1543,.T.);
#2936=EDGE_CURVE('',#2428,#2428,#2105,.T.);
#2937=EDGE_CURVE('',#2428,#2427,#1544,.T.);
#2938=EDGE_CURVE('',#2429,#2430,#1545,.T.);
#2939=EDGE_CURVE('',#2430,#2431,#1546,.T.);
#2940=EDGE_CURVE('',#2431,#2432,#1547,.T.);
#2941=EDGE_CURVE('',#2429,#2432,#1548,.T.);
#2942=EDGE_CURVE('',#2430,#2433,#1549,.T.);
#2943=EDGE_CURVE('',#2433,#2434,#1550,.T.);
#2944=EDGE_CURVE('',#2434,#2431,#1551,.T.);
#2945=EDGE_CURVE('',#2433,#2435,#1552,.T.);
#2946=EDGE_CURVE('',#2435,#2436,#1553,.T.);
#2947=EDGE_CURVE('',#2436,#2434,#1554,.T.);
#2948=EDGE_CURVE('',#2435,#2437,#1555,.T.);
#2949=EDGE_CURVE('',#2437,#2438,#1556,.T.);
#2950=EDGE_CURVE('',#2438,#2436,#1557,.T.);
#2951=EDGE_CURVE('',#2437,#2439,#1558,.T.);
#2952=EDGE_CURVE('',#2439,#2440,#1559,.T.);
#2953=EDGE_CURVE('',#2440,#2438,#1560,.T.);
#2954=EDGE_CURVE('',#2439,#2429,#1561,.T.);
#2955=EDGE_CURVE('',#2432,#2440,#1562,.T.);
#3912=ORIENTED_EDGE('',*,*,#2924,.F.);
#3913=ORIENTED_EDGE('',*,*,#2925,.F.);
#3914=ORIENTED_EDGE('',*,*,#2926,.T.);
#3915=ORIENTED_EDGE('',*,*,#2924,.T.);
#3916=ORIENTED_EDGE('',*,*,#2926,.F.);
#3917=ORIENTED_EDGE('',*,*,#2927,.F.);
#3918=ORIENTED_EDGE('',*,*,#2928,.T.);
#3919=ORIENTED_EDGE('',*,*,#2925,.T.);
#3920=ORIENTED_EDGE('',*,*,#2928,.F.);
#3921=ORIENTED_EDGE('',*,*,#2929,.F.);
#3922=ORIENTED_EDGE('',*,*,#2930,.T.);
#3923=ORIENTED_EDGE('',*,*,#2927,.T.);
#3924=ORIENTED_EDGE('',*,*,#2930,.F.);
#3925=ORIENTED_EDGE('',*,*,#2929,.T.);
#3926=ORIENTED_EDGE('',*,*,#2931,.F.);
#3927=ORIENTED_EDGE('',*,*,#2932,.F.);
#3928=ORIENTED_EDGE('',*,*,#2933,.T.);
#3929=ORIENTED_EDGE('',*,*,#2931,.T.);
#3930=ORIENTED_EDGE('',*,*,#2933,.F.);
#3931=ORIENTED_EDGE('',*,*,#2934,.F.);
#3932=ORIENTED_EDGE('',*,*,#2935,.T.);
#3933=ORIENTED_EDGE('',*,*,#2932,.T.);
#3934=ORIENTED_EDGE('',*,*,#2935,.F.);
#3935=ORIENTED_EDGE('',*,*,#2936,.F.);
#3936=ORIENTED_EDGE('',*,*,#2937,.T.);
#3937=ORIENTED_EDGE('',*,*,#2934,.T.);
#3938=ORIENTED_EDGE('',*,*,#2937,.F.);
#3939=ORIENTED_EDGE('',*,*,#2936,.T.);
#3940=ORIENTED_EDGE('',*,*,#2938,.T.);
#3941=ORIENTED_EDGE('',*,*,#2939,.T.);
#3942=ORIENTED_EDGE('',*,*,#2940,.T.);
#3943=ORIENTED_EDGE('',*,*,#2941,.F.);
#3944=ORIENTED_EDGE('',*,*,#2942,.T.);
#3945=ORIENTED_EDGE('',*,*,#2943,.T.);
#3946=ORIENTED_EDGE('',*,*,#2944,.T.);
#3947=ORIENTED_EDGE('',*,*,#2939,.F.);
#3948=ORIENTED_EDGE('',*,*,#2945,.T.);
#3949=ORIENTED_EDGE('',*,*,#2946,.T.);
#3950=ORIENTED_EDGE('',*,*,#2947,.T.);
#3951=ORIENTED_EDGE('',*,*,#2943,.F.);
#3952=ORIENTED_EDGE('',*,*,#2948,.T.);
#3953=ORIENTED_EDGE('',*,*,#2949,.T.);
#3954=ORIENTED_EDGE('',*,*,#2950,.T.);
#3955=ORIENTED_EDGE('',*,*,#2946,.F.);
#3956=ORIENTED_EDGE('',*,*,#2951,.T.);
#3957=ORIENTED_EDGE('',*,*,#2952,.T.);
#3958=ORIENTED_EDGE('',*,*,#2953,.T.);
#3959=ORIENTED_EDGE('',*,*,#2949,.F.);
#3960=ORIENTED_EDGE('',*,*,#2954,.T.);
#3961=ORIENTED_EDGE('',*,*,#2941,.T.);
#3962=ORIENTED_EDGE('',*,*,#2955,.T.);
#3963=ORIENTED_EDGE('',*,*,#2952,.F.);
#3964=ORIENTED_EDGE('',*,*,#2954,.F.);
#3965=ORIENTED_EDGE('',*,*,#2951,.F.);
#3966=ORIENTED_EDGE('',*,*,#2948,.F.);
#3967=ORIENTED_EDGE('',*,*,#2945,.F.);
#3968=ORIENTED_EDGE('',*,*,#2942,.F.);
#3969=ORIENTED_EDGE('',*,*,#2938,.F.);
#3970=ORIENTED_EDGE('',*,*,#2955,.F.);
#3971=ORIENTED_EDGE('',*,*,#2940,.F.);
#3972=ORIENTED_EDGE('',*,*,#2944,.F.);
#3973=ORIENTED_EDGE('',*,*,#2947,.F.);
#3974=ORIENTED_EDGE('',*,*,#2950,.F.);
#3975=ORIENTED_EDGE('',*,*,#2953,.F.);
#4129=CYLINDRICAL_SURFACE('',#5066,0.425);
#4130=CYLINDRICAL_SURFACE('',#5074,0.24505);
#4354=ADVANCED_FACE('',(#835),#592,.T.);
#4355=ADVANCED_FACE('',(#836),#252,.T.);
#4356=ADVANCED_FACE('',(#837),#4129,.T.);
#4357=ADVANCED_FACE('',(#838),#253,.T.);
#4358=ADVANCED_FACE('',(#839,#455),#593,.T.);
#4359=ADVANCED_FACE('',(#840),#254,.T.);
#4360=ADVANCED_FACE('',(#841),#4130,.T.);
#4361=ADVANCED_FACE('',(#842),#255,.T.);
#4362=ADVANCED_FACE('',(#843),#594,.T.);
#4363=ADVANCED_FACE('',(#844),#595,.F.);
#4364=ADVANCED_FACE('',(#845),#596,.F.);
#4365=ADVANCED_FACE('',(#846),#597,.F.);
#4366=ADVANCED_FACE('',(#847),#598,.F.);
#4367=ADVANCED_FACE('',(#848),#599,.F.);
#4368=ADVANCED_FACE('',(#849),#600,.F.);
#4369=ADVANCED_FACE('',(#850),#601,.F.);
#4370=ADVANCED_FACE('',(#851),#602,.F.);
#4412=CLOSED_SHELL('',(#4354,#4355,#4356,#4357,#4358,#4359,#4360,#4361,
#4362));
#4413=CLOSED_SHELL('',(#4363,#4364,#4365,#4366,#4367,#4368,#4369,#4370));
#5061=AXIS2_PLACEMENT_3D('',#7575,#6290,#6291);
#5062=AXIS2_PLACEMENT_3D('',#7576,#6292,#6293);
#5063=AXIS2_PLACEMENT_3D('',#7578,#6294,#6295);
#5064=AXIS2_PLACEMENT_3D('',#7579,#6296,#6297);
#5065=AXIS2_PLACEMENT_3D('',#7581,#6298,#6299);
#5066=AXIS2_PLACEMENT_3D('',#7583,#6301,#6302);
#5067=AXIS2_PLACEMENT_3D('',#7585,#6303,#6304);
#5068=AXIS2_PLACEMENT_3D('',#7587,#6306,#6307);
#5069=AXIS2_PLACEMENT_3D('',#7589,#6308,#6309);
#5070=AXIS2_PLACEMENT_3D('',#7591,#6311,#6312);
#5071=AXIS2_PLACEMENT_3D('',#7593,#6313,#6314);
#5072=AXIS2_PLACEMENT_3D('',#7594,#6315,#6316);
#5073=AXIS2_PLACEMENT_3D('',#7596,#6317,#6318);
#5074=AXIS2_PLACEMENT_3D('',#7598,#6320,#6321);
#5075=AXIS2_PLACEMENT_3D('',#7600,#6322,#6323);
#5076=AXIS2_PLACEMENT_3D('',#7602,#6325,#6326);
#5077=AXIS2_PLACEMENT_3D('',#7604,#6327,#6328);
#5078=AXIS2_PLACEMENT_3D('',#7606,#6330,#6331);
#5079=AXIS2_PLACEMENT_3D('',#7607,#6332,#6333);
#5080=AXIS2_PLACEMENT_3D('',#7616,#6338,#6339);
#5081=AXIS2_PLACEMENT_3D('',#7622,#6343,#6344);
#5082=AXIS2_PLACEMENT_3D('',#7628,#6348,#6349);
#5083=AXIS2_PLACEMENT_3D('',#7634,#6353,#6354);
#5084=AXIS2_PLACEMENT_3D('',#7640,#6358,#6359);
#5085=AXIS2_PLACEMENT_3D('',#7643,#6362,#6363);
#5086=AXIS2_PLACEMENT_3D('',#7644,#6364,#6365);
#6290=DIRECTION('axis',(0.,0.,1.));
#6291=DIRECTION('refdir',(1.,0.,0.));
#6292=DIRECTION('center_axis',(0.,1.,0.));
#6293=DIRECTION('ref_axis',(0.,0.,1.));
#6294=DIRECTION('center_axis',(0.,-1.,0.));
#6295=DIRECTION('ref_axis',(1.,0.,0.));
#6296=DIRECTION('center_axis',(0.,-1.,0.));
#6297=DIRECTION('ref_axis',(1.,0.,0.));
#6298=DIRECTION('center_axis',(0.,-1.,0.));
#6299=DIRECTION('ref_axis',(1.,0.,0.));
#6300=DIRECTION('',(0.707106781186548,0.707106781186547,8.65956056235493E-17));
#6301=DIRECTION('center_axis',(0.,-1.,0.));
#6302=DIRECTION('ref_axis',(1.,0.,0.));
#6303=DIRECTION('center_axis',(0.,-1.,0.));
#6304=DIRECTION('ref_axis',(1.,0.,0.));
#6305=DIRECTION('',(0.,1.,0.));
#6306=DIRECTION('center_axis',(0.,1.,0.));
#6307=DIRECTION('ref_axis',(1.,0.,0.));
#6308=DIRECTION('center_axis',(0.,-1.,0.));
#6309=DIRECTION('ref_axis',(1.,0.,0.));
#6310=DIRECTION('',(-0.707106781186547,0.707106781186548,-8.65956056235493E-17));
#6311=DIRECTION('center_axis',(0.,-1.,0.));
#6312=DIRECTION('ref_axis',(0.,0.,-1.));
#6313=DIRECTION('center_axis',(0.,-1.,0.));
#6314=DIRECTION('ref_axis',(1.,0.,0.));
#6315=DIRECTION('center_axis',(0.,1.,0.));
#6316=DIRECTION('ref_axis',(1.,0.,0.));
#6317=DIRECTION('center_axis',(0.,1.,0.));
#6318=DIRECTION('ref_axis',(1.,0.,0.));
#6319=DIRECTION('',(-0.447213595499958,0.894427190999916,-5.47678698264203E-17));
#6320=DIRECTION('center_axis',(0.,-1.,0.));
#6321=DIRECTION('ref_axis',(1.,0.,0.));
#6322=DIRECTION('center_axis',(0.,1.,0.));
#6323=DIRECTION('ref_axis',(1.,0.,0.));
#6324=DIRECTION('',(0.,1.,0.));
#6325=DIRECTION('center_axis',(0.,1.,0.));
#6326=DIRECTION('ref_axis',(1.,0.,0.));
#6327=DIRECTION('center_axis',(0.,-1.,0.));
#6328=DIRECTION('ref_axis',(1.,0.,0.));
#6329=DIRECTION('',(-0.707106781186547,0.707106781186548,-8.65956056235493E-17));
#6330=DIRECTION('center_axis',(0.,-1.,0.));
#6331=DIRECTION('ref_axis',(0.,0.,-1.));
#6332=DIRECTION('center_axis',(0.866025403784439,0.,-0.5));
#6333=DIRECTION('ref_axis',(0.5,0.,0.866025403784439));
#6334=DIRECTION('',(-0.5,0.,-0.866025403784439));
#6335=DIRECTION('',(0.,-1.,0.));
#6336=DIRECTION('',(0.5,0.,0.866025403784439));
#6337=DIRECTION('',(0.,-1.,0.));
#6338=DIRECTION('center_axis',(1.20185167898973E-16,0.,-1.));
#6339=DIRECTION('ref_axis',(1.,0.,1.20185167898973E-16));
#6340=DIRECTION('',(-1.,0.,-1.20185167898973E-16));
#6341=DIRECTION('',(0.,-1.,0.));
#6342=DIRECTION('',(1.,0.,1.20185167898973E-16));
#6343=DIRECTION('center_axis',(-0.866025403784439,0.,-0.5));
#6344=DIRECTION('ref_axis',(0.5,0.,-0.866025403784439));
#6345=DIRECTION('',(-0.5,0.,0.866025403784439));
#6346=DIRECTION('',(0.,-1.,0.));
#6347=DIRECTION('',(0.5,0.,-0.866025403784439));
#6348=DIRECTION('center_axis',(-0.866025403784439,0.,0.5));
#6349=DIRECTION('ref_axis',(-0.5,0.,-0.866025403784439));
#6350=DIRECTION('',(0.5,0.,0.866025403784439));
#6351=DIRECTION('',(0.,-1.,0.));
#6352=DIRECTION('',(-0.5,0.,-0.866025403784439));
#6353=DIRECTION('center_axis',(-2.40370335797945E-16,0.,1.));
#6354=DIRECTION('ref_axis',(-1.,0.,-2.40370335797945E-16));
#6355=DIRECTION('',(1.,0.,2.40370335797945E-16));
#6356=DIRECTION('',(0.,-1.,0.));
#6357=DIRECTION('',(-1.,0.,-2.40370335797945E-16));
#6358=DIRECTION('center_axis',(0.866025403784439,0.,0.5));
#6359=DIRECTION('ref_axis',(-0.5,0.,0.866025403784439));
#6360=DIRECTION('',(0.5,0.,-0.866025403784439));
#6361=DIRECTION('',(-0.5,0.,0.866025403784439));
#6362=DIRECTION('center_axis',(0.,1.,0.));
#6363=DIRECTION('ref_axis',(1.,0.,0.));
#6364=DIRECTION('center_axis',(0.,-1.,0.));
#6365=DIRECTION('ref_axis',(0.,0.,-1.));
#7575=CARTESIAN_POINT('',(0.,0.,0.));
#7576=CARTESIAN_POINT('Origin',(0.375,0.5,0.));
#7577=CARTESIAN_POINT('',(-0.375,0.5,-4.59242549680257E-17));
#7578=CARTESIAN_POINT('Origin',(0.,0.5,0.));
#7579=CARTESIAN_POINT('Origin',(0.,0.475,0.));
#7580=CARTESIAN_POINT('',(-0.425,0.45,-5.20474889637625E-17));
#7581=CARTESIAN_POINT('Origin',(0.,0.45,0.));
#7582=CARTESIAN_POINT('',(-0.4,0.475,-4.89858719658941E-17));
#7583=CARTESIAN_POINT('Origin',(0.,0.24,0.));
#7584=CARTESIAN_POINT('',(-0.425,0.0299999999999998,-5.20474889637625E-17));
#7585=CARTESIAN_POINT('Origin',(0.,0.0299999999999998,0.));
#7586=CARTESIAN_POINT('',(-0.425,0.24,-5.20474889637625E-17));
#7587=CARTESIAN_POINT('Origin',(0.,0.0150000000000001,0.));
#7588=CARTESIAN_POINT('',(-0.395,4.85722573273506E-17,-4.83735485663204E-17));
#7589=CARTESIAN_POINT('Origin',(0.,0.,0.));
#7590=CARTESIAN_POINT('',(-0.41,0.0150000000000001,-5.02105187650415E-17));
#7591=CARTESIAN_POINT('Origin',(0.27,0.,0.));
#7592=CARTESIAN_POINT('',(-0.27,0.,-3.30654635769785E-17));
#7593=CARTESIAN_POINT('Origin',(0.,0.,0.));
#7594=CARTESIAN_POINT('Origin',(0.,-0.02,0.));
#7595=CARTESIAN_POINT('',(-0.24505,-0.0498999999999999,3.00099698131059E-17));
#7596=CARTESIAN_POINT('Origin',(0.,-0.0498999999999999,0.));
#7597=CARTESIAN_POINT('',(-0.26,-0.02,-3.18408167778312E-17));
#7598=CARTESIAN_POINT('Origin',(0.,-0.995,0.));
#7599=CARTESIAN_POINT('',(-0.24505,-1.95495,3.00099698131059E-17));
#7600=CARTESIAN_POINT('Origin',(0.,-1.95495,0.));
#7601=CARTESIAN_POINT('',(-0.24505,-0.995,-3.00099698131059E-17));
#7602=CARTESIAN_POINT('Origin',(0.,-1.975,0.));
#7603=CARTESIAN_POINT('',(-0.2,-2.,-2.44929359829471E-17));
#7604=CARTESIAN_POINT('Origin',(0.,-2.,0.));
#7605=CARTESIAN_POINT('',(-0.225,-1.975,-2.75545529808154E-17));
#7606=CARTESIAN_POINT('Origin',(0.,-2.,0.));
#7607=CARTESIAN_POINT('Origin',(0.115470053837925,-0.5,-0.2));
#7608=CARTESIAN_POINT('',(0.23094010767585,-0.5,0.));
#7609=CARTESIAN_POINT('',(0.115470053837925,-0.5,-0.2));
#7610=CARTESIAN_POINT('',(0.23094010767585,-0.5,0.));
#7611=CARTESIAN_POINT('',(0.115470053837925,-0.8,-0.2));
#7612=CARTESIAN_POINT('',(0.115470053837925,-0.5,-0.2));
#7613=CARTESIAN_POINT('',(0.23094010767585,-0.8,0.));
#7614=CARTESIAN_POINT('',(0.23094010767585,-0.8,0.));
#7615=CARTESIAN_POINT('',(0.23094010767585,-0.5,0.));
#7616=CARTESIAN_POINT('Origin',(-0.115470053837925,-0.5,-0.2));
#7617=CARTESIAN_POINT('',(-0.115470053837925,-0.5,-0.2));
#7618=CARTESIAN_POINT('',(0.115470053837925,-0.5,-0.2));
#7619=CARTESIAN_POINT('',(-0.115470053837925,-0.8,-0.2));
#7620=CARTESIAN_POINT('',(-0.115470053837925,-0.5,-0.2));
#7621=CARTESIAN_POINT('',(0.115470053837925,-0.8,-0.2));
#7622=CARTESIAN_POINT('Origin',(-0.23094010767585,-0.5,-2.77555756156289E-17));
#7623=CARTESIAN_POINT('',(-0.23094010767585,-0.5,-2.82820063659975E-17));
#7624=CARTESIAN_POINT('',(-0.115470053837925,-0.5,-0.2));
#7625=CARTESIAN_POINT('',(-0.23094010767585,-0.8,-2.77555756156289E-17));
#7626=CARTESIAN_POINT('',(-0.23094010767585,-0.5,-2.82820063659975E-17));
#7627=CARTESIAN_POINT('',(-0.115470053837925,-0.8,-0.2));
#7628=CARTESIAN_POINT('Origin',(-0.115470053837925,-0.5,0.2));
#7629=CARTESIAN_POINT('',(-0.115470053837925,-0.5,0.2));
#7630=CARTESIAN_POINT('',(-0.23094010767585,-0.5,-2.82820063659975E-17));
#7631=CARTESIAN_POINT('',(-0.115470053837925,-0.8,0.2));
#7632=CARTESIAN_POINT('',(-0.115470053837925,-0.5,0.2));
#7633=CARTESIAN_POINT('',(-0.23094010767585,-0.8,-2.82820063659975E-17));
#7634=CARTESIAN_POINT('Origin',(0.115470053837925,-0.5,0.2));
#7635=CARTESIAN_POINT('',(0.115470053837925,-0.5,0.2));
#7636=CARTESIAN_POINT('',(-0.115470053837925,-0.5,0.2));
#7637=CARTESIAN_POINT('',(0.115470053837925,-0.8,0.2));
#7638=CARTESIAN_POINT('',(0.115470053837925,-0.5,0.2));
#7639=CARTESIAN_POINT('',(-0.115470053837925,-0.8,0.2));
#7640=CARTESIAN_POINT('Origin',(0.23094010767585,-0.5,0.));
#7641=CARTESIAN_POINT('',(0.115470053837925,-0.5,0.2));
#7642=CARTESIAN_POINT('',(0.115470053837925,-0.8,0.2));
#7643=CARTESIAN_POINT('Origin',(0.,-0.5,0.));
#7644=CARTESIAN_POINT('Origin',(0.,-0.8,0.));
#7806=UNCERTAINTY_MEASURE_WITH_UNIT(LENGTH_MEASURE(0.001),#7836,
'DISTANCE_ACCURACY_VALUE',
'Maximum model space distance between geometric entities at asserted c
onnectivities');
#7809=UNCERTAINTY_MEASURE_WITH_UNIT(LENGTH_MEASURE(0.001),#7836,
'DISTANCE_ACCURACY_VALUE',
'Maximum model space distance between geometric entities at asserted c
onnectivities');
#7832=(
GEOMETRIC_REPRESENTATION_CONTEXT(3)
GLOBAL_UNCERTAINTY_ASSIGNED_CONTEXT((#7806))
GLOBAL_UNIT_ASSIGNED_CONTEXT((#7836,#7838,#7839))
REPRESENTATION_CONTEXT('','3D')
);
#7835=(
GEOMETRIC_REPRESENTATION_CONTEXT(3)
GLOBAL_UNCERTAINTY_ASSIGNED_CONTEXT((#7809))
GLOBAL_UNIT_ASSIGNED_CONTEXT((#7836,#7838,#7839))
REPRESENTATION_CONTEXT('','3D')
);
#7836=(
LENGTH_UNIT()
NAMED_UNIT(*)
SI_UNIT(.CENTI.,.METRE.)
);
#7838=(
NAMED_UNIT(*)
PLANE_ANGLE_UNIT()
SI_UNIT($,.RADIAN.)
);
#7839=(
NAMED_UNIT(*)
SI_UNIT($,.STERADIAN.)
SOLID_ANGLE_UNIT()
);
#7862=SHAPE_DEFINITION_REPRESENTATION(#7889,#7968);
#7889=PRODUCT_DEFINITION_SHAPE('',$,#7994);
#7968=SHAPE_REPRESENTATION('',(#5061),#7832);
#7971=PRODUCT_DEFINITION_CONTEXT('part definition',#8048,'design');
#7994=PRODUCT_DEFINITION('Cap Screw - M5x20','Cap Screw - M5x20',#8019,
#7971);
#8019=PRODUCT_DEFINITION_FORMATION('',$,#8072);
#8048=APPLICATION_CONTEXT(
'Core Data for Automotive Mechanical Design Process');
#8049=PRODUCT_CONTEXT('part definition',#8048,'mechanical');
#8072=PRODUCT('Cap Screw - M5x20','Cap Screw - M5x20',
'Cap Screw - M5x20',(#8049));
#8145=COLOUR_RGB('Black',0.12,0.14,0.17);
#8146=FILL_AREA_STYLE_COLOUR('',#8145);
#8147=FILL_AREA_STYLE('',(#8146));
#8148=SURFACE_STYLE_FILL_AREA(#8147);
#8149=SURFACE_SIDE_STYLE('',(#8148));
#8150=SURFACE_STYLE_USAGE(.BOTH.,#8149);
#8151=PRESENTATION_STYLE_ASSIGNMENT((#8150));
ENDSEC;
END-ISO-10303-21;
